ISO-10303-21;
HEADER;
/* Generated by software containing ST-Developer
 * from STEP Tools, Inc. (www.steptools.com) 
 */

FILE_DESCRIPTION(
/* description */ ('STEP AP214'),
/* implementation_level */ '2;1');

FILE_NAME(
/* name */ 'Ball Screw Nut.step',
/* time_stamp */ '2026-11-15T14:49:54-08:00',
/* author */ (''),
/* organization */ (''),
/* preprocessor_version */ 'ST-DEVELOPER v20.2',
/* originating_system */ 'Autodesk Translation Framework v15.17.0.0',
/* authorisation */ '');

FILE_SCHEMA (('AUTOMOTIVE_DESIGN { 1 0 10303 214 3 1 1 }'));
ENDSEC;

DATA;
#10=MECHANICAL_DESIGN_GEOMETRIC_PRESENTATION_REPRESENTATION('',(#1108),#66721);
#73=TOROIDAL_SURFACE('',#27366,17.5,0.5);
#74=TOROIDAL_SURFACE('',#27372,28.,1.);
#75=TOROIDAL_SURFACE('',#27374,28.,1.);
#76=TOROIDAL_SURFACE('',#27380,28.,1.);
#77=TOROIDAL_SURFACE('',#27382,28.,1.);
#118=B_SPLINE_CURVE_WITH_KNOTS('',3,(#39937,#39938,#39939,#39940,#39941,
#39942,#39943,#39944,#39945,#39946,#39947,#39948,#39949,#39950,#39951,#39952,
#39953,#39954,#39955,#39956,#39957,#39958,#39959,#39960,#39961,#39962,#39963,
#39964,#39965,#39966,#39967,#39968,#39969,#39970),.UNSPECIFIED.,.T.,.F.,
(4,2,2,2,2,2,2,2,2,2,2,2,2,2,2,2,4),(0.,0.0926562327783873,0.185312465556775,
0.277968535864378,0.370624606171981,0.463280676479585,0.555936746787188,
0.648592979565575,0.741249212343963,0.83390544512235,0.926561677900738,
1.01921774820834,1.11187381851594,1.20452988882355,1.29718595913115,1.38984219190954,
1.48249842468793),.UNSPECIFIED.);
#119=B_SPLINE_CURVE_WITH_KNOTS('',3,(#39973,#39974,#39975,#39976,#39977,
#39978,#39979,#39980,#39981,#39982,#39983,#39984,#39985,#39986,#39987,#39988,
#39989,#39990,#39991,#39992,#39993,#39994,#39995,#39996,#39997,#39998,#39999,
#40000,#40001,#40002,#40003,#40004,#40005,#40006),.UNSPECIFIED.,.T.,.F.,
(4,2,2,2,2,2,2,2,2,2,2,2,2,2,2,2,4),(0.,0.0930265888637791,0.186053177727558,
0.279067626609053,0.372082075490548,0.465096524372043,0.558110973253538,
0.651137562117317,0.744164150981096,0.837190739844876,0.930217328708655,
1.02323177759015,1.11624622647164,1.20926067535314,1.30227512423463,1.39530171309841,
1.48832830196219),.UNSPECIFIED.);
#120=B_SPLINE_CURVE_WITH_KNOTS('',3,(#40094,#40095,#40096,#40097,#40098,
#40099,#40100,#40101,#40102,#40103),.UNSPECIFIED.,.F.,.F.,(4,2,2,2,4),(-0.786889893332756,
-0.754960430904454,-0.714729481242358,-0.661694768386944,-0.593637938221159),
 .UNSPECIFIED.);
#121=B_SPLINE_CURVE_WITH_KNOTS('',3,(#40106,#40107,#40108,#40109,#40110,
#40111,#40112,#40113,#40114,#40115),.UNSPECIFIED.,.F.,.F.,(4,2,2,2,4),(-0.193251955111595,
-0.125195124945811,-0.0721604120903979,-0.0319294624283026,-2.77555756156289E-17),
 .UNSPECIFIED.);
#122=B_SPLINE_CURVE_WITH_KNOTS('',3,(#40118,#40119,#40120,#40121,#40122,
#40123,#40124,#40125,#40126,#40127),.UNSPECIFIED.,.F.,.F.,(4,2,2,2,4),(-0.193251955111592,
-0.125195124945809,-0.0721604120903967,-0.0319294624283021,0.),
 .UNSPECIFIED.);
#123=B_SPLINE_CURVE_WITH_KNOTS('',3,(#40129,#40130,#40131,#40132,#40133,
#40134,#40135,#40136,#40137,#40138),.UNSPECIFIED.,.F.,.F.,(4,2,2,2,4),(-0.786889893332756,
-0.754960430904454,-0.714729481242359,-0.661694768386946,-0.593637938221162),
 .UNSPECIFIED.);
#124=B_SPLINE_CURVE_WITH_KNOTS('',3,(#40154,#40155,#40156,#40157,#40158,
#40159,#40160,#40161,#40162,#40163),.UNSPECIFIED.,.F.,.F.,(4,2,2,2,4),(-0.193251955111594,
-0.125195124945831,-0.072160412090434,-0.0319294624283508,-5.83144643684363E-14),
 .UNSPECIFIED.);
#125=B_SPLINE_CURVE_WITH_KNOTS('',3,(#40166,#40167,#40168,#40169,#40170,
#40171,#40172,#40173,#40174,#40175),.UNSPECIFIED.,.F.,.F.,(4,2,2,2,4),(-0.786889893332936,
-0.754960430904604,-0.714729481242472,-0.661694768387011,-0.593637938221165),
 .UNSPECIFIED.);
#126=B_SPLINE_CURVE_WITH_KNOTS('',3,(#40178,#40179,#40180,#40181,#40182,
#40183,#40184,#40185,#40186,#40187),.UNSPECIFIED.,.F.,.F.,(4,2,2,2,4),(-0.786889893332757,
-0.754960430904455,-0.71472948124236,-0.661694768386948,-0.593637938221165),
 .UNSPECIFIED.);
#127=B_SPLINE_CURVE_WITH_KNOTS('',3,(#40189,#40190,#40191,#40192,#40193,
#40194,#40195,#40196,#40197,#40198),.UNSPECIFIED.,.F.,.F.,(4,2,2,2,4),(-0.193251955111592,
-0.125195124945673,-0.0721604120901549,-0.0319294624279794,3.86274345842708E-13),
 .UNSPECIFIED.);
#1046=SHAPE_REPRESENTATION_RELATIONSHIP('SRR','None',#66905,#1077);
#1077=ADVANCED_BREP_SHAPE_REPRESENTATION('',(#1143),#66696);
#1108=STYLED_ITEM('',(#67095),#1143);
#1143=MANIFOLD_SOLID_BREP('Body1',#25674);
#1307=FACE_BOUND('',#4498,.T.);
#1308=FACE_BOUND('',#4503,.T.);
#1309=FACE_BOUND('',#4504,.T.);
#1310=FACE_BOUND('',#4505,.T.);
#1311=FACE_BOUND('',#4506,.T.);
#1312=FACE_BOUND('',#4507,.T.);
#1313=FACE_BOUND('',#4508,.T.);
#1314=FACE_BOUND('',#4509,.T.);
#1315=FACE_BOUND('',#4513,.T.);
#1316=FACE_BOUND('',#4518,.T.);
#1317=FACE_BOUND('',#4519,.T.);
#1318=FACE_BOUND('',#4520,.T.);
#1319=FACE_BOUND('',#4521,.T.);
#1320=FACE_BOUND('',#4522,.T.);
#1321=FACE_BOUND('',#4523,.T.);
#1322=FACE_BOUND('',#4524,.T.);
#1323=FACE_BOUND('',#4526,.T.);
#1324=FACE_BOUND('',#4528,.T.);
#1325=FACE_BOUND('',#4530,.T.);
#1326=FACE_BOUND('',#4532,.T.);
#1327=FACE_BOUND('',#4534,.T.);
#1880=PLANE('',#27369);
#1881=PLANE('',#27384);
#1882=PLANE('',#27385);
#1883=PLANE('',#27386);
#1884=PLANE('',#27387);
#1885=PLANE('',#27388);
#1886=PLANE('',#27389);
#1887=PLANE('',#27390);
#1888=PLANE('',#27391);
#2906=FACE_OUTER_BOUND('',#4487,.T.);
#2907=FACE_OUTER_BOUND('',#4488,.T.);
#2908=FACE_OUTER_BOUND('',#4489,.T.);
#2909=FACE_OUTER_BOUND('',#4490,.T.);
#2910=FACE_OUTER_BOUND('',#4491,.T.);
#2911=FACE_OUTER_BOUND('',#4492,.T.);
#2912=FACE_OUTER_BOUND('',#4493,.T.);
#2913=FACE_OUTER_BOUND('',#4494,.T.);
#2914=FACE_OUTER_BOUND('',#4495,.T.);
#2915=FACE_OUTER_BOUND('',#4496,.T.);
#2916=FACE_OUTER_BOUND('',#4497,.T.);
#2917=FACE_OUTER_BOUND('',#4499,.T.);
#2918=FACE_OUTER_BOUND('',#4500,.T.);
#2919=FACE_OUTER_BOUND('',#4501,.T.);
#2920=FACE_OUTER_BOUND('',#4502,.T.);
#2921=FACE_OUTER_BOUND('',#4510,.T.);
#2922=FACE_OUTER_BOUND('',#4511,.T.);
#2923=FACE_OUTER_BOUND('',#4512,.T.);
#2924=FACE_OUTER_BOUND('',#4514,.T.);
#2925=FACE_OUTER_BOUND('',#4515,.T.);
#2926=FACE_OUTER_BOUND('',#4516,.T.);
#2927=FACE_OUTER_BOUND('',#4517,.T.);
#2928=FACE_OUTER_BOUND('',#4525,.T.);
#2929=FACE_OUTER_BOUND('',#4527,.T.);
#2930=FACE_OUTER_BOUND('',#4529,.T.);
#2931=FACE_OUTER_BOUND('',#4531,.T.);
#2932=FACE_OUTER_BOUND('',#4533,.T.);
#2933=FACE_OUTER_BOUND('',#4535,.T.);
#2934=FACE_OUTER_BOUND('',#4536,.T.);
#4487=EDGE_LOOP('',(#20086,#20087,#20088,#20089));
#4488=EDGE_LOOP('',(#20090,#20091,#20092,#20093));
#4489=EDGE_LOOP('',(#20094,#20095,#20096,#20097));
#4490=EDGE_LOOP('',(#20098,#20099,#20100,#20101));
#4491=EDGE_LOOP('',(#20102,#20103,#20104,#20105));
#4492=EDGE_LOOP('',(#20106,#20107,#20108,#20109));
#4493=EDGE_LOOP('',(#20110,#20111,#20112,#20113));
#4494=EDGE_LOOP('',(#20114,#20115,#20116,#20117));
#4495=EDGE_LOOP('',(#20118,#20119,#20120,#20121));
#4496=EDGE_LOOP('',(#20122,#20123,#20124,#20125));
#4497=EDGE_LOOP('',(#20126,#20127,#20128,#20129));
#4498=EDGE_LOOP('',(#20130));
#4499=EDGE_LOOP('',(#20131,#20132,#20133,#20134));
#4500=EDGE_LOOP('',(#20135,#20136,#20137,#20138));
#4501=EDGE_LOOP('',(#20139,#20140,#20141,#20142));
#4502=EDGE_LOOP('',(#20143,#20144,#20145,#20146));
#4503=EDGE_LOOP('',(#20147));
#4504=EDGE_LOOP('',(#20148));
#4505=EDGE_LOOP('',(#20149));
#4506=EDGE_LOOP('',(#20150));
#4507=EDGE_LOOP('',(#20151));
#4508=EDGE_LOOP('',(#20152));
#4509=EDGE_LOOP('',(#20153));
#4510=EDGE_LOOP('',(#20154,#20155,#20156,#20157));
#4511=EDGE_LOOP('',(#20158,#20159,#20160,#20161));
#4512=EDGE_LOOP('',(#20162,#20163,#20164,#20165));
#4513=EDGE_LOOP('',(#20166));
#4514=EDGE_LOOP('',(#20167,#20168,#20169,#20170));
#4515=EDGE_LOOP('',(#20171,#20172,#20173,#20174));
#4516=EDGE_LOOP('',(#20175,#20176,#20177,#20178));
#4517=EDGE_LOOP('',(#20179,#20180,#20181,#20182));
#4518=EDGE_LOOP('',(#20183));
#4519=EDGE_LOOP('',(#20184));
#4520=EDGE_LOOP('',(#20185));
#4521=EDGE_LOOP('',(#20186));
#4522=EDGE_LOOP('',(#20187));
#4523=EDGE_LOOP('',(#20188));
#4524=EDGE_LOOP('',(#20189));
#4525=EDGE_LOOP('',(#20190));
#4526=EDGE_LOOP('',(#20191));
#4527=EDGE_LOOP('',(#20192));
#4528=EDGE_LOOP('',(#20193));
#4529=EDGE_LOOP('',(#20194));
#4530=EDGE_LOOP('',(#20195));
#4531=EDGE_LOOP('',(#20196));
#4532=EDGE_LOOP('',(#20197));
#4533=EDGE_LOOP('',(#20198));
#4534=EDGE_LOOP('',(#20199));
#4535=EDGE_LOOP('',(#20200,#20201,#20202,#20203,#20204,#20205,#20206,#20207));
#4536=EDGE_LOOP('',(#20208,#20209,#20210,#20211,#20212,#20213,#20214,#20215));
#6568=LINE('',#39972,#8557);
#6569=LINE('',#40011,#8558);
#6570=LINE('',#40017,#8559);
#6571=LINE('',#40023,#8560);
#6572=LINE('',#40029,#8561);
#6573=LINE('',#40035,#8562);
#6574=LINE('',#40041,#8563);
#6575=LINE('',#40047,#8564);
#6576=LINE('',#40053,#8565);
#6577=LINE('',#40059,#8566);
#6578=LINE('',#40065,#8567);
#6579=LINE('',#40071,#8568);
#6580=LINE('',#40077,#8569);
#6581=LINE('',#40086,#8570);
#6582=LINE('',#40090,#8571);
#6583=LINE('',#40142,#8572);
#6584=LINE('',#40145,#8573);
#6585=LINE('',#40148,#8574);
#6586=LINE('',#40150,#8575);
#6587=LINE('',#40201,#8576);
#6588=LINE('',#40202,#8577);
#8557=VECTOR('',#32419,2.45849999999999);
#8558=VECTOR('',#32424,3.3);
#8559=VECTOR('',#32431,3.3);
#8560=VECTOR('',#32438,3.3);
#8561=VECTOR('',#32445,3.3);
#8562=VECTOR('',#32452,3.3);
#8563=VECTOR('',#32459,3.3);
#8564=VECTOR('',#32466,18.);
#8565=VECTOR('',#32473,13.);
#8566=VECTOR('',#32480,12.75);
#8567=VECTOR('',#32487,10.);
#8568=VECTOR('',#32494,12.75);
#8569=VECTOR('',#32501,13.);
#8570=VECTOR('',#32512,1000.);
#8571=VECTOR('',#32515,1000.);
#8572=VECTOR('',#32528,1000.);
#8573=VECTOR('',#32531,1000.);
#8574=VECTOR('',#32534,1000.);
#8575=VECTOR('',#32535,1000.);
#8576=VECTOR('',#32548,1000.);
#8577=VECTOR('',#32549,1000.);
#10010=CIRCLE('',#27331,3.3);
#10011=CIRCLE('',#27332,3.29999999999999);
#10012=CIRCLE('',#27334,3.3);
#10013=CIRCLE('',#27335,3.29999999999999);
#10014=CIRCLE('',#27337,3.3);
#10015=CIRCLE('',#27338,3.3);
#10016=CIRCLE('',#27340,3.3);
#10017=CIRCLE('',#27341,3.3);
#10018=CIRCLE('',#27343,3.3);
#10019=CIRCLE('',#27344,3.29999999999999);
#10020=CIRCLE('',#27346,3.3);
#10021=CIRCLE('',#27347,3.3);
#10022=CIRCLE('',#27349,18.);
#10023=CIRCLE('',#27350,18.);
#10024=CIRCLE('',#27352,13.);
#10025=CIRCLE('',#27353,13.);
#10026=CIRCLE('',#27355,12.75);
#10027=CIRCLE('',#27356,12.75);
#10028=CIRCLE('',#27358,10.);
#10029=CIRCLE('',#27359,10.);
#10030=CIRCLE('',#27361,12.75);
#10031=CIRCLE('',#27362,12.75);
#10032=CIRCLE('',#27364,13.);
#10033=CIRCLE('',#27365,13.);
#10034=CIRCLE('',#27367,17.5);
#10035=CIRCLE('',#27368,0.5);
#10036=CIRCLE('',#27370,28.);
#10037=CIRCLE('',#27371,28.);
#10038=CIRCLE('',#27373,29.);
#10039=CIRCLE('',#27375,29.);
#10040=CIRCLE('',#27377,29.);
#10041=CIRCLE('',#27379,29.);
#10042=CIRCLE('',#27381,28.);
#10043=CIRCLE('',#27383,28.);
#11792=VERTEX_POINT('',#39936);
#11793=VERTEX_POINT('',#39971);
#11794=VERTEX_POINT('',#40008);
#11795=VERTEX_POINT('',#40010);
#11796=VERTEX_POINT('',#40014);
#11797=VERTEX_POINT('',#40016);
#11798=VERTEX_POINT('',#40020);
#11799=VERTEX_POINT('',#40022);
#11800=VERTEX_POINT('',#40026);
#11801=VERTEX_POINT('',#40028);
#11802=VERTEX_POINT('',#40032);
#11803=VERTEX_POINT('',#40034);
#11804=VERTEX_POINT('',#40038);
#11805=VERTEX_POINT('',#40040);
#11806=VERTEX_POINT('',#40044);
#11807=VERTEX_POINT('',#40046);
#11808=VERTEX_POINT('',#40050);
#11809=VERTEX_POINT('',#40052);
#11810=VERTEX_POINT('',#40056);
#11811=VERTEX_POINT('',#40058);
#11812=VERTEX_POINT('',#40062);
#11813=VERTEX_POINT('',#40064);
#11814=VERTEX_POINT('',#40068);
#11815=VERTEX_POINT('',#40070);
#11816=VERTEX_POINT('',#40074);
#11817=VERTEX_POINT('',#40076);
#11818=VERTEX_POINT('',#40080);
#11819=VERTEX_POINT('',#40084);
#11820=VERTEX_POINT('',#40085);
#11821=VERTEX_POINT('',#40087);
#11822=VERTEX_POINT('',#40089);
#11823=VERTEX_POINT('',#40093);
#11824=VERTEX_POINT('',#40104);
#11825=VERTEX_POINT('',#40117);
#11826=VERTEX_POINT('',#40128);
#11827=VERTEX_POINT('',#40141);
#11828=VERTEX_POINT('',#40143);
#11829=VERTEX_POINT('',#40147);
#11830=VERTEX_POINT('',#40149);
#11831=VERTEX_POINT('',#40153);
#11832=VERTEX_POINT('',#40164);
#11833=VERTEX_POINT('',#40177);
#11834=VERTEX_POINT('',#40188);
#14736=EDGE_CURVE('',#11792,#11792,#118,.T.);
#14737=EDGE_CURVE('',#11792,#11793,#6568,.T.);
#14738=EDGE_CURVE('',#11793,#11793,#119,.T.);
#14739=EDGE_CURVE('',#11794,#11794,#10010,.T.);
#14740=EDGE_CURVE('',#11794,#11795,#6569,.T.);
#14741=EDGE_CURVE('',#11795,#11795,#10011,.T.);
#14742=EDGE_CURVE('',#11796,#11796,#10012,.T.);
#14743=EDGE_CURVE('',#11796,#11797,#6570,.T.);
#14744=EDGE_CURVE('',#11797,#11797,#10013,.T.);
#14745=EDGE_CURVE('',#11798,#11798,#10014,.T.);
#14746=EDGE_CURVE('',#11798,#11799,#6571,.T.);
#14747=EDGE_CURVE('',#11799,#11799,#10015,.T.);
#14748=EDGE_CURVE('',#11800,#11800,#10016,.T.);
#14749=EDGE_CURVE('',#11800,#11801,#6572,.T.);
#14750=EDGE_CURVE('',#11801,#11801,#10017,.T.);
#14751=EDGE_CURVE('',#11802,#11802,#10018,.T.);
#14752=EDGE_CURVE('',#11802,#11803,#6573,.T.);
#14753=EDGE_CURVE('',#11803,#11803,#10019,.T.);
#14754=EDGE_CURVE('',#11804,#11804,#10020,.T.);
#14755=EDGE_CURVE('',#11804,#11805,#6574,.T.);
#14756=EDGE_CURVE('',#11805,#11805,#10021,.T.);
#14757=EDGE_CURVE('',#11806,#11806,#10022,.T.);
#14758=EDGE_CURVE('',#11806,#11807,#6575,.T.);
#14759=EDGE_CURVE('',#11807,#11807,#10023,.T.);
#14760=EDGE_CURVE('',#11808,#11808,#10024,.T.);
#14761=EDGE_CURVE('',#11808,#11809,#6576,.T.);
#14762=EDGE_CURVE('',#11809,#11809,#10025,.T.);
#14763=EDGE_CURVE('',#11810,#11810,#10026,.T.);
#14764=EDGE_CURVE('',#11810,#11811,#6577,.T.);
#14765=EDGE_CURVE('',#11811,#11811,#10027,.T.);
#14766=EDGE_CURVE('',#11812,#11812,#10028,.T.);
#14767=EDGE_CURVE('',#11812,#11813,#6578,.T.);
#14768=EDGE_CURVE('',#11813,#11813,#10029,.T.);
#14769=EDGE_CURVE('',#11814,#11814,#10030,.T.);
#14770=EDGE_CURVE('',#11814,#11815,#6579,.T.);
#14771=EDGE_CURVE('',#11815,#11815,#10031,.T.);
#14772=EDGE_CURVE('',#11816,#11816,#10032,.T.);
#14773=EDGE_CURVE('',#11816,#11817,#6580,.T.);
#14774=EDGE_CURVE('',#11817,#11817,#10033,.T.);
#14775=EDGE_CURVE('',#11818,#11818,#10034,.T.);
#14776=EDGE_CURVE('',#11818,#11806,#10035,.T.);
#14777=EDGE_CURVE('',#11819,#11820,#6581,.T.);
#14778=EDGE_CURVE('',#11821,#11820,#10036,.T.);
#14779=EDGE_CURVE('',#11821,#11822,#6582,.T.);
#14780=EDGE_CURVE('',#11819,#11822,#10037,.T.);
#14781=EDGE_CURVE('',#11823,#11820,#120,.T.);
#14782=EDGE_CURVE('',#11824,#11823,#10038,.T.);
#14783=EDGE_CURVE('',#11821,#11824,#121,.T.);
#14784=EDGE_CURVE('',#11819,#11825,#122,.T.);
#14785=EDGE_CURVE('',#11826,#11822,#123,.T.);
#14786=EDGE_CURVE('',#11825,#11826,#10039,.T.);
#14787=EDGE_CURVE('',#11827,#11826,#6583,.T.);
#14788=EDGE_CURVE('',#11828,#11827,#10040,.T.);
#14789=EDGE_CURVE('',#11825,#11828,#6584,.T.);
#14790=EDGE_CURVE('',#11824,#11829,#6585,.T.);
#14791=EDGE_CURVE('',#11830,#11823,#6586,.T.);
#14792=EDGE_CURVE('',#11829,#11830,#10041,.T.);
#14793=EDGE_CURVE('',#11831,#11830,#124,.T.);
#14794=EDGE_CURVE('',#11832,#11831,#10042,.T.);
#14795=EDGE_CURVE('',#11829,#11832,#125,.T.);
#14796=EDGE_CURVE('',#11828,#11833,#126,.T.);
#14797=EDGE_CURVE('',#11834,#11827,#127,.T.);
#14798=EDGE_CURVE('',#11833,#11834,#10043,.T.);
#14799=EDGE_CURVE('',#11833,#11831,#6587,.T.);
#14800=EDGE_CURVE('',#11832,#11834,#6588,.T.);
#20086=ORIENTED_EDGE('',*,*,#14736,.F.);
#20087=ORIENTED_EDGE('',*,*,#14737,.T.);
#20088=ORIENTED_EDGE('',*,*,#14738,.F.);
#20089=ORIENTED_EDGE('',*,*,#14737,.F.);
#20090=ORIENTED_EDGE('',*,*,#14739,.F.);
#20091=ORIENTED_EDGE('',*,*,#14740,.T.);
#20092=ORIENTED_EDGE('',*,*,#14741,.T.);
#20093=ORIENTED_EDGE('',*,*,#14740,.F.);
#20094=ORIENTED_EDGE('',*,*,#14742,.F.);
#20095=ORIENTED_EDGE('',*,*,#14743,.T.);
#20096=ORIENTED_EDGE('',*,*,#14744,.T.);
#20097=ORIENTED_EDGE('',*,*,#14743,.F.);
#20098=ORIENTED_EDGE('',*,*,#14745,.F.);
#20099=ORIENTED_EDGE('',*,*,#14746,.T.);
#20100=ORIENTED_EDGE('',*,*,#14747,.T.);
#20101=ORIENTED_EDGE('',*,*,#14746,.F.);
#20102=ORIENTED_EDGE('',*,*,#14748,.F.);
#20103=ORIENTED_EDGE('',*,*,#14749,.T.);
#20104=ORIENTED_EDGE('',*,*,#14750,.T.);
#20105=ORIENTED_EDGE('',*,*,#14749,.F.);
#20106=ORIENTED_EDGE('',*,*,#14751,.F.);
#20107=ORIENTED_EDGE('',*,*,#14752,.T.);
#20108=ORIENTED_EDGE('',*,*,#14753,.T.);
#20109=ORIENTED_EDGE('',*,*,#14752,.F.);
#20110=ORIENTED_EDGE('',*,*,#14754,.F.);
#20111=ORIENTED_EDGE('',*,*,#14755,.T.);
#20112=ORIENTED_EDGE('',*,*,#14756,.T.);
#20113=ORIENTED_EDGE('',*,*,#14755,.F.);
#20114=ORIENTED_EDGE('',*,*,#14757,.F.);
#20115=ORIENTED_EDGE('',*,*,#14758,.T.);
#20116=ORIENTED_EDGE('',*,*,#14759,.T.);
#20117=ORIENTED_EDGE('',*,*,#14758,.F.);
#20118=ORIENTED_EDGE('',*,*,#14760,.F.);
#20119=ORIENTED_EDGE('',*,*,#14761,.T.);
#20120=ORIENTED_EDGE('',*,*,#14762,.T.);
#20121=ORIENTED_EDGE('',*,*,#14761,.F.);
#20122=ORIENTED_EDGE('',*,*,#14763,.F.);
#20123=ORIENTED_EDGE('',*,*,#14764,.T.);
#20124=ORIENTED_EDGE('',*,*,#14765,.T.);
#20125=ORIENTED_EDGE('',*,*,#14764,.F.);
#20126=ORIENTED_EDGE('',*,*,#14766,.F.);
#20127=ORIENTED_EDGE('',*,*,#14767,.T.);
#20128=ORIENTED_EDGE('',*,*,#14768,.T.);
#20129=ORIENTED_EDGE('',*,*,#14767,.F.);
#20130=ORIENTED_EDGE('',*,*,#14738,.T.);
#20131=ORIENTED_EDGE('',*,*,#14769,.F.);
#20132=ORIENTED_EDGE('',*,*,#14770,.T.);
#20133=ORIENTED_EDGE('',*,*,#14771,.T.);
#20134=ORIENTED_EDGE('',*,*,#14770,.F.);
#20135=ORIENTED_EDGE('',*,*,#14772,.F.);
#20136=ORIENTED_EDGE('',*,*,#14773,.T.);
#20137=ORIENTED_EDGE('',*,*,#14774,.T.);
#20138=ORIENTED_EDGE('',*,*,#14773,.F.);
#20139=ORIENTED_EDGE('',*,*,#14775,.F.);
#20140=ORIENTED_EDGE('',*,*,#14776,.T.);
#20141=ORIENTED_EDGE('',*,*,#14757,.T.);
#20142=ORIENTED_EDGE('',*,*,#14776,.F.);
#20143=ORIENTED_EDGE('',*,*,#14777,.T.);
#20144=ORIENTED_EDGE('',*,*,#14778,.F.);
#20145=ORIENTED_EDGE('',*,*,#14779,.T.);
#20146=ORIENTED_EDGE('',*,*,#14780,.F.);
#20147=ORIENTED_EDGE('',*,*,#14753,.F.);
#20148=ORIENTED_EDGE('',*,*,#14750,.F.);
#20149=ORIENTED_EDGE('',*,*,#14747,.F.);
#20150=ORIENTED_EDGE('',*,*,#14744,.F.);
#20151=ORIENTED_EDGE('',*,*,#14741,.F.);
#20152=ORIENTED_EDGE('',*,*,#14756,.F.);
#20153=ORIENTED_EDGE('',*,*,#14760,.T.);
#20154=ORIENTED_EDGE('',*,*,#14781,.F.);
#20155=ORIENTED_EDGE('',*,*,#14782,.F.);
#20156=ORIENTED_EDGE('',*,*,#14783,.F.);
#20157=ORIENTED_EDGE('',*,*,#14778,.T.);
#20158=ORIENTED_EDGE('',*,*,#14784,.F.);
#20159=ORIENTED_EDGE('',*,*,#14780,.T.);
#20160=ORIENTED_EDGE('',*,*,#14785,.F.);
#20161=ORIENTED_EDGE('',*,*,#14786,.F.);
#20162=ORIENTED_EDGE('',*,*,#14787,.F.);
#20163=ORIENTED_EDGE('',*,*,#14788,.F.);
#20164=ORIENTED_EDGE('',*,*,#14789,.F.);
#20165=ORIENTED_EDGE('',*,*,#14786,.T.);
#20166=ORIENTED_EDGE('',*,*,#14736,.T.);
#20167=ORIENTED_EDGE('',*,*,#14790,.F.);
#20168=ORIENTED_EDGE('',*,*,#14782,.T.);
#20169=ORIENTED_EDGE('',*,*,#14791,.F.);
#20170=ORIENTED_EDGE('',*,*,#14792,.F.);
#20171=ORIENTED_EDGE('',*,*,#14793,.F.);
#20172=ORIENTED_EDGE('',*,*,#14794,.F.);
#20173=ORIENTED_EDGE('',*,*,#14795,.F.);
#20174=ORIENTED_EDGE('',*,*,#14792,.T.);
#20175=ORIENTED_EDGE('',*,*,#14796,.F.);
#20176=ORIENTED_EDGE('',*,*,#14788,.T.);
#20177=ORIENTED_EDGE('',*,*,#14797,.F.);
#20178=ORIENTED_EDGE('',*,*,#14798,.F.);
#20179=ORIENTED_EDGE('',*,*,#14799,.F.);
#20180=ORIENTED_EDGE('',*,*,#14798,.T.);
#20181=ORIENTED_EDGE('',*,*,#14800,.F.);
#20182=ORIENTED_EDGE('',*,*,#14794,.T.);
#20183=ORIENTED_EDGE('',*,*,#14739,.T.);
#20184=ORIENTED_EDGE('',*,*,#14742,.T.);
#20185=ORIENTED_EDGE('',*,*,#14745,.T.);
#20186=ORIENTED_EDGE('',*,*,#14748,.T.);
#20187=ORIENTED_EDGE('',*,*,#14751,.T.);
#20188=ORIENTED_EDGE('',*,*,#14754,.T.);
#20189=ORIENTED_EDGE('',*,*,#14759,.F.);
#20190=ORIENTED_EDGE('',*,*,#14775,.T.);
#20191=ORIENTED_EDGE('',*,*,#14774,.F.);
#20192=ORIENTED_EDGE('',*,*,#14772,.T.);
#20193=ORIENTED_EDGE('',*,*,#14771,.F.);
#20194=ORIENTED_EDGE('',*,*,#14769,.T.);
#20195=ORIENTED_EDGE('',*,*,#14768,.F.);
#20196=ORIENTED_EDGE('',*,*,#14765,.F.);
#20197=ORIENTED_EDGE('',*,*,#14766,.T.);
#20198=ORIENTED_EDGE('',*,*,#14762,.F.);
#20199=ORIENTED_EDGE('',*,*,#14763,.T.);
#20200=ORIENTED_EDGE('',*,*,#14783,.T.);
#20201=ORIENTED_EDGE('',*,*,#14790,.T.);
#20202=ORIENTED_EDGE('',*,*,#14795,.T.);
#20203=ORIENTED_EDGE('',*,*,#14800,.T.);
#20204=ORIENTED_EDGE('',*,*,#14797,.T.);
#20205=ORIENTED_EDGE('',*,*,#14787,.T.);
#20206=ORIENTED_EDGE('',*,*,#14785,.T.);
#20207=ORIENTED_EDGE('',*,*,#14779,.F.);
#20208=ORIENTED_EDGE('',*,*,#14781,.T.);
#20209=ORIENTED_EDGE('',*,*,#14777,.F.);
#20210=ORIENTED_EDGE('',*,*,#14784,.T.);
#20211=ORIENTED_EDGE('',*,*,#14789,.T.);
#20212=ORIENTED_EDGE('',*,*,#14796,.T.);
#20213=ORIENTED_EDGE('',*,*,#14799,.T.);
#20214=ORIENTED_EDGE('',*,*,#14793,.T.);
#20215=ORIENTED_EDGE('',*,*,#14791,.T.);
#24027=CYLINDRICAL_SURFACE('',#27329,2.45849999999999);
#24028=CYLINDRICAL_SURFACE('',#27330,3.3);
#24029=CYLINDRICAL_SURFACE('',#27333,3.3);
#24030=CYLINDRICAL_SURFACE('',#27336,3.3);
#24031=CYLINDRICAL_SURFACE('',#27339,3.3);
#24032=CYLINDRICAL_SURFACE('',#27342,3.3);
#24033=CYLINDRICAL_SURFACE('',#27345,3.3);
#24034=CYLINDRICAL_SURFACE('',#27348,18.);
#24035=CYLINDRICAL_SURFACE('',#27351,13.);
#24036=CYLINDRICAL_SURFACE('',#27354,12.75);
#24037=CYLINDRICAL_SURFACE('',#27357,10.);
#24038=CYLINDRICAL_SURFACE('',#27360,12.75);
#24039=CYLINDRICAL_SURFACE('',#27363,13.);
#24040=CYLINDRICAL_SURFACE('',#27376,29.);
#24041=CYLINDRICAL_SURFACE('',#27378,29.);
#24859=ADVANCED_FACE('',(#2906),#24027,.F.);
#24860=ADVANCED_FACE('',(#2907),#24028,.F.);
#24861=ADVANCED_FACE('',(#2908),#24029,.F.);
#24862=ADVANCED_FACE('',(#2909),#24030,.F.);
#24863=ADVANCED_FACE('',(#2910),#24031,.F.);
#24864=ADVANCED_FACE('',(#2911),#24032,.F.);
#24865=ADVANCED_FACE('',(#2912),#24033,.F.);
#24866=ADVANCED_FACE('',(#2913),#24034,.T.);
#24867=ADVANCED_FACE('',(#2914),#24035,.F.);
#24868=ADVANCED_FACE('',(#2915),#24036,.T.);
#24869=ADVANCED_FACE('',(#2916,#1307),#24037,.F.);
#24870=ADVANCED_FACE('',(#2917),#24038,.T.);
#24871=ADVANCED_FACE('',(#2918),#24039,.F.);
#24872=ADVANCED_FACE('',(#2919),#73,.T.);
#24873=ADVANCED_FACE('',(#2920,#1308,#1309,#1310,#1311,#1312,#1313,#1314),
#1880,.F.);
#24874=ADVANCED_FACE('',(#2921),#74,.T.);
#24875=ADVANCED_FACE('',(#2922),#75,.T.);
#24876=ADVANCED_FACE('',(#2923,#1315),#24040,.T.);
#24877=ADVANCED_FACE('',(#2924),#24041,.T.);
#24878=ADVANCED_FACE('',(#2925),#76,.T.);
#24879=ADVANCED_FACE('',(#2926),#77,.T.);
#24880=ADVANCED_FACE('',(#2927,#1316,#1317,#1318,#1319,#1320,#1321,#1322),
#1881,.F.);
#24881=ADVANCED_FACE('',(#2928,#1323),#1882,.F.);
#24882=ADVANCED_FACE('',(#2929,#1324),#1883,.F.);
#24883=ADVANCED_FACE('',(#2930,#1325),#1884,.F.);
#24884=ADVANCED_FACE('',(#2931,#1326),#1885,.F.);
#24885=ADVANCED_FACE('',(#2932,#1327),#1886,.F.);
#24886=ADVANCED_FACE('',(#2933),#1887,.T.);
#24887=ADVANCED_FACE('',(#2934),#1888,.T.);
#25674=CLOSED_SHELL('',(#24859,#24860,#24861,#24862,#24863,#24864,#24865,
#24866,#24867,#24868,#24869,#24870,#24871,#24872,#24873,#24874,#24875,#24876,
#24877,#24878,#24879,#24880,#24881,#24882,#24883,#24884,#24885,#24886,#24887));
#27328=AXIS2_PLACEMENT_3D('',#39934,#32415,#32416);
#27329=AXIS2_PLACEMENT_3D('',#39935,#32417,#32418);
#27330=AXIS2_PLACEMENT_3D('',#40007,#32420,#32421);
#27331=AXIS2_PLACEMENT_3D('',#40009,#32422,#32423);
#27332=AXIS2_PLACEMENT_3D('',#40012,#32425,#32426);
#27333=AXIS2_PLACEMENT_3D('',#40013,#32427,#32428);
#27334=AXIS2_PLACEMENT_3D('',#40015,#32429,#32430);
#27335=AXIS2_PLACEMENT_3D('',#40018,#32432,#32433);
#27336=AXIS2_PLACEMENT_3D('',#40019,#32434,#32435);
#27337=AXIS2_PLACEMENT_3D('',#40021,#32436,#32437);
#27338=AXIS2_PLACEMENT_3D('',#40024,#32439,#32440);
#27339=AXIS2_PLACEMENT_3D('',#40025,#32441,#32442);
#27340=AXIS2_PLACEMENT_3D('',#40027,#32443,#32444);
#27341=AXIS2_PLACEMENT_3D('',#40030,#32446,#32447);
#27342=AXIS2_PLACEMENT_3D('',#40031,#32448,#32449);
#27343=AXIS2_PLACEMENT_3D('',#40033,#32450,#32451);
#27344=AXIS2_PLACEMENT_3D('',#40036,#32453,#32454);
#27345=AXIS2_PLACEMENT_3D('',#40037,#32455,#32456);
#27346=AXIS2_PLACEMENT_3D('',#40039,#32457,#32458);
#27347=AXIS2_PLACEMENT_3D('',#40042,#32460,#32461);
#27348=AXIS2_PLACEMENT_3D('',#40043,#32462,#32463);
#27349=AXIS2_PLACEMENT_3D('',#40045,#32464,#32465);
#27350=AXIS2_PLACEMENT_3D('',#40048,#32467,#32468);
#27351=AXIS2_PLACEMENT_3D('',#40049,#32469,#32470);
#27352=AXIS2_PLACEMENT_3D('',#40051,#32471,#32472);
#27353=AXIS2_PLACEMENT_3D('',#40054,#32474,#32475);
#27354=AXIS2_PLACEMENT_3D('',#40055,#32476,#32477);
#27355=AXIS2_PLACEMENT_3D('',#40057,#32478,#32479);
#27356=AXIS2_PLACEMENT_3D('',#40060,#32481,#32482);
#27357=AXIS2_PLACEMENT_3D('',#40061,#32483,#32484);
#27358=AXIS2_PLACEMENT_3D('',#40063,#32485,#32486);
#27359=AXIS2_PLACEMENT_3D('',#40066,#32488,#32489);
#27360=AXIS2_PLACEMENT_3D('',#40067,#32490,#32491);
#27361=AXIS2_PLACEMENT_3D('',#40069,#32492,#32493);
#27362=AXIS2_PLACEMENT_3D('',#40072,#32495,#32496);
#27363=AXIS2_PLACEMENT_3D('',#40073,#32497,#32498);
#27364=AXIS2_PLACEMENT_3D('',#40075,#32499,#32500);
#27365=AXIS2_PLACEMENT_3D('',#40078,#32502,#32503);
#27366=AXIS2_PLACEMENT_3D('',#40079,#32504,#32505);
#27367=AXIS2_PLACEMENT_3D('',#40081,#32506,#32507);
#27368=AXIS2_PLACEMENT_3D('',#40082,#32508,#32509);
#27369=AXIS2_PLACEMENT_3D('',#40083,#32510,#32511);
#27370=AXIS2_PLACEMENT_3D('',#40088,#32513,#32514);
#27371=AXIS2_PLACEMENT_3D('',#40091,#32516,#32517);
#27372=AXIS2_PLACEMENT_3D('',#40092,#32518,#32519);
#27373=AXIS2_PLACEMENT_3D('',#40105,#32520,#32521);
#27374=AXIS2_PLACEMENT_3D('',#40116,#32522,#32523);
#27375=AXIS2_PLACEMENT_3D('',#40139,#32524,#32525);
#27376=AXIS2_PLACEMENT_3D('',#40140,#32526,#32527);
#27377=AXIS2_PLACEMENT_3D('',#40144,#32529,#32530);
#27378=AXIS2_PLACEMENT_3D('',#40146,#32532,#32533);
#27379=AXIS2_PLACEMENT_3D('',#40151,#32536,#32537);
#27380=AXIS2_PLACEMENT_3D('',#40152,#32538,#32539);
#27381=AXIS2_PLACEMENT_3D('',#40165,#32540,#32541);
#27382=AXIS2_PLACEMENT_3D('',#40176,#32542,#32543);
#27383=AXIS2_PLACEMENT_3D('',#40199,#32544,#32545);
#27384=AXIS2_PLACEMENT_3D('',#40200,#32546,#32547);
#27385=AXIS2_PLACEMENT_3D('',#40203,#32550,#32551);
#27386=AXIS2_PLACEMENT_3D('',#40204,#32552,#32553);
#27387=AXIS2_PLACEMENT_3D('',#40205,#32554,#32555);
#27388=AXIS2_PLACEMENT_3D('',#40206,#32556,#32557);
#27389=AXIS2_PLACEMENT_3D('',#40207,#32558,#32559);
#27390=AXIS2_PLACEMENT_3D('',#40208,#32560,#32561);
#27391=AXIS2_PLACEMENT_3D('',#40209,#32562,#32563);
#32415=DIRECTION('axis',(0.,0.,1.));
#32416=DIRECTION('refdir',(1.,0.,0.));
#32417=DIRECTION('center_axis',(0.,-0.923879532511287,-0.382683432365091));
#32418=DIRECTION('ref_axis',(0.,0.382683432365091,-0.923879532511286));
#32419=DIRECTION('',(0.,-0.923879532511286,-0.382683432365091));
#32420=DIRECTION('center_axis',(1.,0.,0.));
#32421=DIRECTION('ref_axis',(0.,0.,-1.));
#32422=DIRECTION('center_axis',(1.,0.,0.));
#32423=DIRECTION('ref_axis',(0.,0.,-1.));
#32424=DIRECTION('',(1.,0.,0.));
#32425=DIRECTION('center_axis',(1.,0.,0.));
#32426=DIRECTION('ref_axis',(0.,0.,-1.));
#32427=DIRECTION('center_axis',(1.,0.,0.));
#32428=DIRECTION('ref_axis',(0.,0.,-1.));
#32429=DIRECTION('center_axis',(1.,0.,0.));
#32430=DIRECTION('ref_axis',(0.,0.,-1.));
#32431=DIRECTION('',(1.,0.,0.));
#32432=DIRECTION('center_axis',(1.,0.,0.));
#32433=DIRECTION('ref_axis',(0.,0.,-1.));
#32434=DIRECTION('center_axis',(1.,0.,0.));
#32435=DIRECTION('ref_axis',(0.,0.,-1.));
#32436=DIRECTION('center_axis',(1.,0.,0.));
#32437=DIRECTION('ref_axis',(0.,0.,-1.));
#32438=DIRECTION('',(1.,0.,0.));
#32439=DIRECTION('center_axis',(1.,0.,0.));
#32440=DIRECTION('ref_axis',(0.,0.,-1.));
#32441=DIRECTION('center_axis',(1.,0.,0.));
#32442=DIRECTION('ref_axis',(0.,0.,-1.));
#32443=DIRECTION('center_axis',(1.,0.,0.));
#32444=DIRECTION('ref_axis',(0.,0.,-1.));
#32445=DIRECTION('',(1.,0.,0.));
#32446=DIRECTION('center_axis',(1.,0.,0.));
#32447=DIRECTION('ref_axis',(0.,0.,-1.));
#32448=DIRECTION('center_axis',(1.,0.,0.));
#32449=DIRECTION('ref_axis',(0.,0.,-1.));
#32450=DIRECTION('center_axis',(1.,0.,0.));
#32451=DIRECTION('ref_axis',(0.,0.,-1.));
#32452=DIRECTION('',(1.,0.,0.));
#32453=DIRECTION('center_axis',(1.,0.,0.));
#32454=DIRECTION('ref_axis',(0.,0.,-1.));
#32455=DIRECTION('center_axis',(1.,0.,0.));
#32456=DIRECTION('ref_axis',(0.,0.,-1.));
#32457=DIRECTION('center_axis',(1.,0.,0.));
#32458=DIRECTION('ref_axis',(0.,0.,-1.));
#32459=DIRECTION('',(1.,0.,0.));
#32460=DIRECTION('center_axis',(1.,0.,0.));
#32461=DIRECTION('ref_axis',(0.,0.,-1.));
#32462=DIRECTION('center_axis',(-1.,0.,0.));
#32463=DIRECTION('ref_axis',(0.,0.,1.));
#32464=DIRECTION('center_axis',(-1.,0.,0.));
#32465=DIRECTION('ref_axis',(0.,0.,1.));
#32466=DIRECTION('',(1.,0.,0.));
#32467=DIRECTION('center_axis',(-1.,0.,0.));
#32468=DIRECTION('ref_axis',(0.,0.,1.));
#32469=DIRECTION('center_axis',(-1.,0.,0.));
#32470=DIRECTION('ref_axis',(0.,0.,1.));
#32471=DIRECTION('center_axis',(-1.,0.,0.));
#32472=DIRECTION('ref_axis',(0.,0.,1.));
#32473=DIRECTION('',(-1.,0.,0.));
#32474=DIRECTION('center_axis',(-1.,0.,0.));
#32475=DIRECTION('ref_axis',(0.,0.,1.));
#32476=DIRECTION('center_axis',(-1.,0.,0.));
#32477=DIRECTION('ref_axis',(0.,0.,1.));
#32478=DIRECTION('center_axis',(-1.,0.,0.));
#32479=DIRECTION('ref_axis',(0.,0.,1.));
#32480=DIRECTION('',(1.,0.,0.));
#32481=DIRECTION('center_axis',(-1.,0.,0.));
#32482=DIRECTION('ref_axis',(0.,0.,1.));
#32483=DIRECTION('center_axis',(-1.,0.,0.));
#32484=DIRECTION('ref_axis',(0.,0.,1.));
#32485=DIRECTION('center_axis',(-1.,0.,0.));
#32486=DIRECTION('ref_axis',(0.,0.,1.));
#32487=DIRECTION('',(-1.,0.,0.));
#32488=DIRECTION('center_axis',(-1.,0.,0.));
#32489=DIRECTION('ref_axis',(0.,0.,1.));
#32490=DIRECTION('center_axis',(-1.,0.,0.));
#32491=DIRECTION('ref_axis',(0.,0.,1.));
#32492=DIRECTION('center_axis',(-1.,0.,0.));
#32493=DIRECTION('ref_axis',(0.,0.,1.));
#32494=DIRECTION('',(1.,0.,0.));
#32495=DIRECTION('center_axis',(-1.,0.,0.));
#32496=DIRECTION('ref_axis',(0.,0.,1.));
#32497=DIRECTION('center_axis',(-1.,0.,0.));
#32498=DIRECTION('ref_axis',(0.,0.,1.));
#32499=DIRECTION('center_axis',(-1.,0.,0.));
#32500=DIRECTION('ref_axis',(0.,0.,1.));
#32501=DIRECTION('',(-1.,0.,0.));
#32502=DIRECTION('center_axis',(-1.,0.,0.));
#32503=DIRECTION('ref_axis',(0.,0.,1.));
#32504=DIRECTION('center_axis',(-1.,0.,0.));
#32505=DIRECTION('ref_axis',(0.,0.,1.));
#32506=DIRECTION('center_axis',(-1.,0.,0.));
#32507=DIRECTION('ref_axis',(0.,0.,1.));
#32508=DIRECTION('center_axis',(0.,-1.,1.22464679914735E-16));
#32509=DIRECTION('ref_axis',(0.,-1.22464679914735E-16,-1.));
#32510=DIRECTION('center_axis',(-1.,0.,0.));
#32511=DIRECTION('ref_axis',(0.,0.,1.));
#32512=DIRECTION('',(0.,-1.,1.19636101791504E-16));
#32513=DIRECTION('center_axis',(-1.,0.,0.));
#32514=DIRECTION('ref_axis',(0.,0.,1.));
#32515=DIRECTION('',(0.,1.,1.19636101791504E-16));
#32516=DIRECTION('center_axis',(-1.,0.,0.));
#32517=DIRECTION('ref_axis',(0.,0.,1.));
#32518=DIRECTION('center_axis',(-1.,0.,0.));
#32519=DIRECTION('ref_axis',(0.,0.,1.));
#32520=DIRECTION('center_axis',(-1.,0.,0.));
#32521=DIRECTION('ref_axis',(0.,0.,1.));
#32522=DIRECTION('center_axis',(-1.,0.,0.));
#32523=DIRECTION('ref_axis',(0.,0.,1.));
#32524=DIRECTION('center_axis',(-1.,0.,0.));
#32525=DIRECTION('ref_axis',(0.,0.,1.));
#32526=DIRECTION('center_axis',(-1.,0.,0.));
#32527=DIRECTION('ref_axis',(0.,0.,1.));
#32528=DIRECTION('',(1.,0.,0.));
#32529=DIRECTION('center_axis',(-1.,0.,0.));
#32530=DIRECTION('ref_axis',(0.,0.,1.));
#32531=DIRECTION('',(-1.,0.,0.));
#32532=DIRECTION('center_axis',(-1.,0.,0.));
#32533=DIRECTION('ref_axis',(0.,0.,1.));
#32534=DIRECTION('',(-1.,0.,0.));
#32535=DIRECTION('',(1.,0.,0.));
#32536=DIRECTION('center_axis',(-1.,0.,0.));
#32537=DIRECTION('ref_axis',(0.,0.,1.));
#32538=DIRECTION('center_axis',(-1.,0.,0.));
#32539=DIRECTION('ref_axis',(0.,0.,1.));
#32540=DIRECTION('center_axis',(-1.,0.,0.));
#32541=DIRECTION('ref_axis',(0.,0.,1.));
#32542=DIRECTION('center_axis',(-1.,0.,0.));
#32543=DIRECTION('ref_axis',(0.,0.,1.));
#32544=DIRECTION('center_axis',(-1.,0.,0.));
#32545=DIRECTION('ref_axis',(0.,0.,1.));
#32546=DIRECTION('center_axis',(1.,0.,0.));
#32547=DIRECTION('ref_axis',(0.,0.,-1.));
#32548=DIRECTION('',(0.,-1.,1.19636101791504E-16));
#32549=DIRECTION('',(0.,1.,1.19636101791504E-16));
#32550=DIRECTION('center_axis',(1.,0.,0.));
#32551=DIRECTION('ref_axis',(0.,0.,-1.));
#32552=DIRECTION('center_axis',(1.,0.,0.));
#32553=DIRECTION('ref_axis',(0.,0.,-1.));
#32554=DIRECTION('center_axis',(1.,0.,0.));
#32555=DIRECTION('ref_axis',(0.,0.,-1.));
#32556=DIRECTION('center_axis',(-1.,0.,0.));
#32557=DIRECTION('ref_axis',(0.,0.,1.));
#32558=DIRECTION('center_axis',(-1.,0.,0.));
#32559=DIRECTION('ref_axis',(0.,0.,1.));
#32560=DIRECTION('center_axis',(0.,1.19636101791504E-16,-1.));
#32561=DIRECTION('ref_axis',(0.,1.,1.19636101791504E-16));
#32562=DIRECTION('center_axis',(0.,1.19636101791504E-16,1.));
#32563=DIRECTION('ref_axis',(0.,-1.,1.19636101791504E-16));
#39934=CARTESIAN_POINT('',(0.,0.,0.));
#39935=CARTESIAN_POINT('Origin',(5.,0.,0.));
#39936=CARTESIAN_POINT('',(5.,25.755227454346,13.3292257380129));
#39937=CARTESIAN_POINT('Ctrl Pts',(5.,25.755227454346,13.3292257380129));
#39938=CARTESIAN_POINT('Ctrl Pts',(4.69114589073871,25.755227454346,13.3292257380129));
#39939=CARTESIAN_POINT('Ctrl Pts',(4.36180679068939,25.7839061219684,13.2742617732837));
#39940=CARTESIAN_POINT('Ctrl Pts',(3.75612725368286,25.8981524209919,13.0499632820151));
#39941=CARTESIAN_POINT('Ctrl Pts',(3.47977417462311,25.9834526414702,12.8805267791833));
#39942=CARTESIAN_POINT('Ctrl Pts',(3.04338216488515,26.1746646562439,12.4873820813809));
#39943=CARTESIAN_POINT('Ctrl Pts',(2.85419996970905,26.2933036476544,12.2374013605568));
#39944=CARTESIAN_POINT('Ctrl Pts',(2.60325479232307,26.5432548470335,11.6853511240012));
#39945=CARTESIAN_POINT('Ctrl Pts',(2.54150000000001,26.6743132994447,11.3831630283214));
#39946=CARTESIAN_POINT('Ctrl Pts',(2.54150000000001,26.9106995862099,10.8124760488539));
#39947=CARTESIAN_POINT('Ctrl Pts',(2.60325479232307,27.0317065174271,10.5061244767731));
#39948=CARTESIAN_POINT('Ctrl Pts',(2.85419996970905,27.2453227952046,9.93902382290224));
#39949=CARTESIAN_POINT('Ctrl Pts',(3.04338216488515,27.3381954227257,9.67837032470212));
#39950=CARTESIAN_POINT('Ctrl Pts',(3.47977417462311,27.4809833922385,9.26516773060774));
#39951=CARTESIAN_POINT('Ctrl Pts',(3.75612725368287,27.5404767280345,9.08504166613792));
#39952=CARTESIAN_POINT('Ctrl Pts',(4.36180679068939,27.6182953794554,8.84565434918702));
#39953=CARTESIAN_POINT('Ctrl Pts',(4.69114589073871,27.6368818912851,8.78651007665487));
#39954=CARTESIAN_POINT('Ctrl Pts',(5.30885410926129,27.6368818912851,8.78651007665487));
#39955=CARTESIAN_POINT('Ctrl Pts',(5.63819320931061,27.6182953794554,8.84565434918702));
#39956=CARTESIAN_POINT('Ctrl Pts',(6.24387274631713,27.5404767280345,9.08504166613792));
#39957=CARTESIAN_POINT('Ctrl Pts',(6.52022582537689,27.4809833922385,9.26516773060774));
#39958=CARTESIAN_POINT('Ctrl Pts',(6.95661783511485,27.3381954227257,9.67837032470212));
#39959=CARTESIAN_POINT('Ctrl Pts',(7.14580003029095,27.2453227952046,9.93902382290224));
#39960=CARTESIAN_POINT('Ctrl Pts',(7.39674520767693,27.0317065174271,10.5061244767731));
#39961=CARTESIAN_POINT('Ctrl Pts',(7.45849999999999,26.9106995862099,10.8124760488539));
#39962=CARTESIAN_POINT('Ctrl Pts',(7.45849999999999,26.6743132994447,11.3831630283214));
#39963=CARTESIAN_POINT('Ctrl Pts',(7.39674520767693,26.5432548470335,11.6853511240012));
#39964=CARTESIAN_POINT('Ctrl Pts',(7.14580003029096,26.2933036476544,12.2374013605568));
#39965=CARTESIAN_POINT('Ctrl Pts',(6.95661783511486,26.1746646562439,12.4873820813809));
#39966=CARTESIAN_POINT('Ctrl Pts',(6.5202258253769,25.9834526414702,12.8805267791833));
#39967=CARTESIAN_POINT('Ctrl Pts',(6.24387274631714,25.8981524209919,13.0499632820151));
#39968=CARTESIAN_POINT('Ctrl Pts',(5.63819320931061,25.7839061219684,13.2742617732837));
#39969=CARTESIAN_POINT('Ctrl Pts',(5.30885410926129,25.755227454346,13.3292257380129));
#39970=CARTESIAN_POINT('Ctrl Pts',(5.,25.755227454346,13.3292257380129));
#39971=CARTESIAN_POINT('',(5.,8.0144099455781,5.98073851829512));
#39972=CARTESIAN_POINT('',(5.,-0.940827218469573,2.27135783067899));
#39973=CARTESIAN_POINT('Ctrl Pts',(5.,8.0144099455781,5.98073851829512));
#39974=CARTESIAN_POINT('Ctrl Pts',(5.31008862954593,8.0144099455781,5.98073851829512));
#39975=CARTESIAN_POINT('Ctrl Pts',(5.63993188917898,8.05340386084043,5.92953036554281));
#39976=CARTESIAN_POINT('Ctrl Pts',(6.24525180858305,8.20369315504142,5.71979564999168));
#39977=CARTESIAN_POINT('Ctrl Pts',(6.52084478062663,8.31410726259137,5.56097433266262));
#39978=CARTESIAN_POINT('Ctrl Pts',(6.95597086860858,8.55158864293188,5.18836525743534));
#39979=CARTESIAN_POINT('Ctrl Pts',(7.14497843142093,8.69464171404924,4.94930727333218));
#39980=CARTESIAN_POINT('Ctrl Pts',(7.39627742385398,8.97925658890556,4.41195966959874));
#39981=CARTESIAN_POINT('Ctrl Pts',(7.45849999999999,9.12014502992114,4.11328147548234));
#39982=CARTESIAN_POINT('Ctrl Pts',(7.45849999999999,9.35744562030459,3.54038717181947));
#39983=CARTESIAN_POINT('Ctrl Pts',(7.39627742385398,9.46901982472393,3.22956662333429));
#39984=CARTESIAN_POINT('Ctrl Pts',(7.14497843142093,9.64772885114073,2.64835138084258));
#39985=CARTESIAN_POINT('Ctrl Pts',(6.95597086860858,9.71561457614021,2.3781580625298));
#39986=CARTESIAN_POINT('Ctrl Pts',(6.52084478062663,9.81116428552076,1.94675896426062));
#39987=CARTESIAN_POINT('Ctrl Pts',(6.24525180858306,9.84539335181388,1.75638076959303));
#39988=CARTESIAN_POINT('Ctrl Pts',(5.63993188917898,9.88742761236105,1.50180535090734));
#39989=CARTESIAN_POINT('Ctrl Pts',(5.31008862954593,9.89606438251724,1.43802285693714));
#39990=CARTESIAN_POINT('Ctrl Pts',(4.68991137045407,9.89606438251724,1.43802285693714));
#39991=CARTESIAN_POINT('Ctrl Pts',(4.36006811082102,9.88742761236105,1.50180535090734));
#39992=CARTESIAN_POINT('Ctrl Pts',(3.75474819141694,9.84539335181388,1.75638076959303));
#39993=CARTESIAN_POINT('Ctrl Pts',(3.47915521937337,9.81116428552076,1.94675896426062));
#39994=CARTESIAN_POINT('Ctrl Pts',(3.04402913139142,9.71561457614021,2.3781580625298));
#39995=CARTESIAN_POINT('Ctrl Pts',(2.85502156857907,9.64772885114073,2.64835138084258));
#39996=CARTESIAN_POINT('Ctrl Pts',(2.60372257614602,9.46901982472393,3.22956662333429));
#39997=CARTESIAN_POINT('Ctrl Pts',(2.54150000000001,9.35744562030459,3.54038717181947));
#39998=CARTESIAN_POINT('Ctrl Pts',(2.54150000000001,9.12014502992114,4.11328147548234));
#39999=CARTESIAN_POINT('Ctrl Pts',(2.60372257614602,8.97925658890556,4.41195966959874));
#40000=CARTESIAN_POINT('Ctrl Pts',(2.85502156857907,8.69464171404924,4.94930727333218));
#40001=CARTESIAN_POINT('Ctrl Pts',(3.04402913139142,8.55158864293188,5.18836525743534));
#40002=CARTESIAN_POINT('Ctrl Pts',(3.47915521937337,8.31410726259137,5.56097433266262));
#40003=CARTESIAN_POINT('Ctrl Pts',(3.75474819141694,8.20369315504142,5.71979564999168));
#40004=CARTESIAN_POINT('Ctrl Pts',(4.36006811082102,8.05340386084043,5.92953036554281));
#40005=CARTESIAN_POINT('Ctrl Pts',(4.68991137045407,8.0144099455781,5.98073851829512));
#40006=CARTESIAN_POINT('Ctrl Pts',(5.,8.0144099455781,5.98073851829512));
#40007=CARTESIAN_POINT('Origin',(10.,16.6170093578838,16.6170093578839));
#40008=CARTESIAN_POINT('',(0.,16.6170093578838,19.9170093578839));
#40009=CARTESIAN_POINT('Origin',(0.,16.6170093578838,16.6170093578839));
#40010=CARTESIAN_POINT('',(10.,16.6170093578838,19.9170093578839));
#40011=CARTESIAN_POINT('',(10.,16.6170093578838,19.9170093578839));
#40012=CARTESIAN_POINT('Origin',(10.,16.6170093578838,16.6170093578839));
#40013=CARTESIAN_POINT('Origin',(10.,23.5,0.));
#40014=CARTESIAN_POINT('',(0.,23.5,3.3));
#40015=CARTESIAN_POINT('Origin',(0.,23.5,0.));
#40016=CARTESIAN_POINT('',(10.,23.5,3.3));
#40017=CARTESIAN_POINT('',(10.,23.5,3.3));
#40018=CARTESIAN_POINT('Origin',(10.,23.5,0.));
#40019=CARTESIAN_POINT('Origin',(10.,16.6170093578838,-16.6170093578839));
#40020=CARTESIAN_POINT('',(0.,16.6170093578838,-13.3170093578839));
#40021=CARTESIAN_POINT('Origin',(0.,16.6170093578838,-16.6170093578839));
#40022=CARTESIAN_POINT('',(10.,16.6170093578838,-13.3170093578839));
#40023=CARTESIAN_POINT('',(10.,16.6170093578838,-13.3170093578839));
#40024=CARTESIAN_POINT('Origin',(10.,16.6170093578838,-16.6170093578839));
#40025=CARTESIAN_POINT('Origin',(10.,-16.6170093578838,16.6170093578839));
#40026=CARTESIAN_POINT('',(0.,-16.6170093578838,19.9170093578839));
#40027=CARTESIAN_POINT('Origin',(0.,-16.6170093578838,16.6170093578839));
#40028=CARTESIAN_POINT('',(10.,-16.6170093578838,19.9170093578839));
#40029=CARTESIAN_POINT('',(10.,-16.6170093578838,19.9170093578839));
#40030=CARTESIAN_POINT('Origin',(10.,-16.6170093578838,16.6170093578839));
#40031=CARTESIAN_POINT('Origin',(10.,-23.5,0.));
#40032=CARTESIAN_POINT('',(0.,-23.5,3.3));
#40033=CARTESIAN_POINT('Origin',(0.,-23.5,0.));
#40034=CARTESIAN_POINT('',(10.,-23.5,3.3));
#40035=CARTESIAN_POINT('',(10.,-23.5,3.3));
#40036=CARTESIAN_POINT('Origin',(10.,-23.5,0.));
#40037=CARTESIAN_POINT('Origin',(10.,-16.6170093578838,-16.6170093578839));
#40038=CARTESIAN_POINT('',(0.,-16.6170093578838,-13.3170093578839));
#40039=CARTESIAN_POINT('Origin',(0.,-16.6170093578838,-16.6170093578839));
#40040=CARTESIAN_POINT('',(10.,-16.6170093578838,-13.3170093578839));
#40041=CARTESIAN_POINT('',(10.,-16.6170093578838,-13.3170093578839));
#40042=CARTESIAN_POINT('Origin',(10.,-16.6170093578838,-16.6170093578839));
#40043=CARTESIAN_POINT('Origin',(-43.5556221990477,0.,0.));
#40044=CARTESIAN_POINT('',(-40.5,-2.20436423846524E-15,-18.));
#40045=CARTESIAN_POINT('Origin',(-40.5,0.,0.));
#40046=CARTESIAN_POINT('',(0.,-2.20436423846524E-15,-18.));
#40047=CARTESIAN_POINT('',(-43.5556221990477,-2.20436423846524E-15,-18.));
#40048=CARTESIAN_POINT('Origin',(0.,0.,0.));
#40049=CARTESIAN_POINT('Origin',(-43.5556221990477,0.,0.));
#40050=CARTESIAN_POINT('',(10.,-1.59204083889156E-15,-13.));
#40051=CARTESIAN_POINT('Origin',(10.,0.,0.));
#40052=CARTESIAN_POINT('',(9.5,-1.59204083889156E-15,-13.));
#40053=CARTESIAN_POINT('',(-43.5556221990477,-1.59204083889156E-15,-13.));
#40054=CARTESIAN_POINT('Origin',(9.5,0.,0.));
#40055=CARTESIAN_POINT('Origin',(-43.5556221990477,0.,0.));
#40056=CARTESIAN_POINT('',(9.5,-1.56142466891288E-15,-12.75));
#40057=CARTESIAN_POINT('Origin',(9.5,0.,0.));
#40058=CARTESIAN_POINT('',(10.,-1.56142466891288E-15,-12.75));
#40059=CARTESIAN_POINT('',(-43.5556221990477,-1.56142466891288E-15,-12.75));
#40060=CARTESIAN_POINT('Origin',(10.,0.,0.));
#40061=CARTESIAN_POINT('Origin',(-43.5556221990477,0.,0.));
#40062=CARTESIAN_POINT('',(10.,-1.22464679914735E-15,-10.));
#40063=CARTESIAN_POINT('Origin',(10.,0.,0.));
#40064=CARTESIAN_POINT('',(-41.,-1.22464679914735E-15,-10.));
#40065=CARTESIAN_POINT('',(-43.5556221990477,-1.22464679914735E-15,-10.));
#40066=CARTESIAN_POINT('Origin',(-41.,0.,0.));
#40067=CARTESIAN_POINT('Origin',(-43.5556221990477,0.,0.));
#40068=CARTESIAN_POINT('',(-41.,-1.56142466891288E-15,-12.75));
#40069=CARTESIAN_POINT('Origin',(-41.,0.,0.));
#40070=CARTESIAN_POINT('',(-40.5,-1.56142466891288E-15,-12.75));
#40071=CARTESIAN_POINT('',(-43.5556221990477,-1.56142466891288E-15,-12.75));
#40072=CARTESIAN_POINT('Origin',(-40.5,0.,0.));
#40073=CARTESIAN_POINT('Origin',(-43.5556221990477,0.,0.));
#40074=CARTESIAN_POINT('',(-40.5,-1.59204083889156E-15,-13.));
#40075=CARTESIAN_POINT('Origin',(-40.5,0.,0.));
#40076=CARTESIAN_POINT('',(-41.,-1.59204083889156E-15,-13.));
#40077=CARTESIAN_POINT('',(-43.5556221990477,-1.59204083889156E-15,-13.));
#40078=CARTESIAN_POINT('Origin',(-41.,0.,0.));
#40079=CARTESIAN_POINT('Origin',(-40.5,0.,0.));
#40080=CARTESIAN_POINT('',(-41.,-2.14313189850787E-15,-17.5));
#40081=CARTESIAN_POINT('Origin',(-41.,0.,0.));
#40082=CARTESIAN_POINT('Origin',(-40.5,-2.14313189850787E-15,-17.5));
#40083=CARTESIAN_POINT('Origin',(10.,28.,0.));
#40084=CARTESIAN_POINT('',(10.,17.3205080756888,22.));
#40085=CARTESIAN_POINT('',(10.,-17.3205080756887,22.));
#40086=CARTESIAN_POINT('',(10.,29.,22.));
#40087=CARTESIAN_POINT('',(10.,-17.3205080756887,-22.));
#40088=CARTESIAN_POINT('Origin',(10.,0.,0.));
#40089=CARTESIAN_POINT('',(10.,17.3205080756888,-22.));
#40090=CARTESIAN_POINT('',(10.,29.,-22.));
#40091=CARTESIAN_POINT('Origin',(10.,0.,0.));
#40092=CARTESIAN_POINT('Origin',(9.,0.,0.));
#40093=CARTESIAN_POINT('',(9.,-18.8944436276912,22.));
#40094=CARTESIAN_POINT('Ctrl Pts',(9.,-18.8944436276912,22.));
#40095=CARTESIAN_POINT('Ctrl Pts',(9.10643154142768,-18.8944436276912,22.));
#40096=CARTESIAN_POINT('Ctrl Pts',(9.22974673696054,-18.8611989035074,22.));
#40097=CARTESIAN_POINT('Ctrl Pts',(9.44255648995507,-18.7490875557919,22.));
#40098=CARTESIAN_POINT('Ctrl Pts',(9.56085821623549,-18.6399950696597,22.));
#40099=CARTESIAN_POINT('Ctrl Pts',(9.75026319887025,-18.3934680475977,22.));
#40100=CARTESIAN_POINT('Ctrl Pts',(9.84146873381169,-18.2019362155735,22.));
#40101=CARTESIAN_POINT('Ctrl Pts',(9.96320710492822,-17.8170936647807,22.));
#40102=CARTESIAN_POINT('Ctrl Pts',(10.,-17.5473641762414,22.));
#40103=CARTESIAN_POINT('Ctrl Pts',(10.,-17.3205080756888,22.));
#40104=CARTESIAN_POINT('',(9.,-18.8944436276912,-22.));
#40105=CARTESIAN_POINT('Origin',(9.,0.,0.));
#40106=CARTESIAN_POINT('Ctrl Pts',(10.,-17.3205080756888,-22.));
#40107=CARTESIAN_POINT('Ctrl Pts',(10.,-17.5473641762414,-22.));
#40108=CARTESIAN_POINT('Ctrl Pts',(9.96320710492822,-17.8170936647807,-22.));
#40109=CARTESIAN_POINT('Ctrl Pts',(9.84146873381169,-18.2019362155735,-22.));
#40110=CARTESIAN_POINT('Ctrl Pts',(9.75026319887025,-18.3934680475977,-22.));
#40111=CARTESIAN_POINT('Ctrl Pts',(9.56085821623549,-18.6399950696597,-22.));
#40112=CARTESIAN_POINT('Ctrl Pts',(9.44255648995507,-18.7490875557919,-22.));
#40113=CARTESIAN_POINT('Ctrl Pts',(9.22974673696054,-18.8611989035074,-22.));
#40114=CARTESIAN_POINT('Ctrl Pts',(9.10643154142768,-18.8944436276912,-22.));
#40115=CARTESIAN_POINT('Ctrl Pts',(9.,-18.8944436276912,-22.));
#40116=CARTESIAN_POINT('Origin',(9.,0.,0.));
#40117=CARTESIAN_POINT('',(9.,18.8944436276912,22.));
#40118=CARTESIAN_POINT('Ctrl Pts',(10.,17.3205080756888,22.));
#40119=CARTESIAN_POINT('Ctrl Pts',(10.,17.5473641762414,22.));
#40120=CARTESIAN_POINT('Ctrl Pts',(9.96320710492822,17.8170936647807,22.));
#40121=CARTESIAN_POINT('Ctrl Pts',(9.84146873381169,18.2019362155735,22.));
#40122=CARTESIAN_POINT('Ctrl Pts',(9.75026319887025,18.3934680475977,22.));
#40123=CARTESIAN_POINT('Ctrl Pts',(9.56085821623549,18.6399950696597,22.));
#40124=CARTESIAN_POINT('Ctrl Pts',(9.44255648995507,18.7490875557919,22.));
#40125=CARTESIAN_POINT('Ctrl Pts',(9.22974673696054,18.8611989035074,22.));
#40126=CARTESIAN_POINT('Ctrl Pts',(9.10643154142768,18.8944436276912,22.));
#40127=CARTESIAN_POINT('Ctrl Pts',(9.,18.8944436276912,22.));
#40128=CARTESIAN_POINT('',(9.,18.8944436276912,-22.));
#40129=CARTESIAN_POINT('Ctrl Pts',(9.,18.8944436276912,-22.));
#40130=CARTESIAN_POINT('Ctrl Pts',(9.10643154142768,18.8944436276912,-22.));
#40131=CARTESIAN_POINT('Ctrl Pts',(9.22974673696054,18.8611989035074,-22.));
#40132=CARTESIAN_POINT('Ctrl Pts',(9.44255648995507,18.7490875557919,-22.));
#40133=CARTESIAN_POINT('Ctrl Pts',(9.56085821623549,18.6399950696597,-22.));
#40134=CARTESIAN_POINT('Ctrl Pts',(9.75026319887025,18.3934680475977,-22.));
#40135=CARTESIAN_POINT('Ctrl Pts',(9.84146873381169,18.2019362155735,-22.));
#40136=CARTESIAN_POINT('Ctrl Pts',(9.96320710492822,17.8170936647807,-22.));
#40137=CARTESIAN_POINT('Ctrl Pts',(10.,17.5473641762414,-22.));
#40138=CARTESIAN_POINT('Ctrl Pts',(10.,17.3205080756888,-22.));
#40139=CARTESIAN_POINT('Origin',(9.,0.,0.));
#40140=CARTESIAN_POINT('Origin',(-43.5556221990477,0.,0.));
#40141=CARTESIAN_POINT('',(1.00000000000386,18.8944436277047,-22.));
#40142=CARTESIAN_POINT('',(-43.5556221990477,18.8944436276912,-22.));
#40143=CARTESIAN_POINT('',(1.,18.8944436276912,22.));
#40144=CARTESIAN_POINT('Origin',(1.,0.,0.));
#40145=CARTESIAN_POINT('',(-43.5556221990477,18.8944436276912,22.));
#40146=CARTESIAN_POINT('Origin',(-43.5556221990477,0.,0.));
#40147=CARTESIAN_POINT('',(1.00000000000179,-18.8944436276974,-22.));
#40148=CARTESIAN_POINT('',(-43.5556221990477,-18.8944436276912,-22.));
#40149=CARTESIAN_POINT('',(0.999999999999417,-18.8944436276931,22.));
#40150=CARTESIAN_POINT('',(-43.5556221990477,-18.8944436276912,22.));
#40151=CARTESIAN_POINT('Origin',(1.,0.,0.));
#40152=CARTESIAN_POINT('Origin',(1.,0.,0.));
#40153=CARTESIAN_POINT('',(1.73472347597681E-15,-17.3205080756888,22.));
#40154=CARTESIAN_POINT('Ctrl Pts',(-4.16333634234434E-16,-17.3205080756888,
22.));
#40155=CARTESIAN_POINT('Ctrl Pts',(-1.14358188512761E-15,-17.5473641762414,
22.));
#40156=CARTESIAN_POINT('Ctrl Pts',(0.0367928950717865,-17.8170936647807,
22.));
#40157=CARTESIAN_POINT('Ctrl Pts',(0.158531266188312,-18.2019362155735,
22.));
#40158=CARTESIAN_POINT('Ctrl Pts',(0.249736801129751,-18.3934680475977,
22.));
#40159=CARTESIAN_POINT('Ctrl Pts',(0.439141783764513,-18.6399950696597,
22.));
#40160=CARTESIAN_POINT('Ctrl Pts',(0.557443510044933,-18.7490875557919,
22.));
#40161=CARTESIAN_POINT('Ctrl Pts',(0.770253263039461,-18.8611989035074,
22.));
#40162=CARTESIAN_POINT('Ctrl Pts',(0.893568458572327,-18.8944436276912,
22.));
#40163=CARTESIAN_POINT('Ctrl Pts',(1.,-18.8944436276912,22.));
#40164=CARTESIAN_POINT('',(0.,-17.3205080756888,-22.));
#40165=CARTESIAN_POINT('Origin',(0.,0.,0.));
#40166=CARTESIAN_POINT('Ctrl Pts',(1.,-18.8944436276912,-22.));
#40167=CARTESIAN_POINT('Ctrl Pts',(0.893568458572327,-18.8944436276912,
-22.));
#40168=CARTESIAN_POINT('Ctrl Pts',(0.770253263039461,-18.8611989035074,
-22.));
#40169=CARTESIAN_POINT('Ctrl Pts',(0.557443510044933,-18.7490875557919,
-22.));
#40170=CARTESIAN_POINT('Ctrl Pts',(0.439141783764514,-18.6399950696597,
-22.));
#40171=CARTESIAN_POINT('Ctrl Pts',(0.249736801129751,-18.3934680475977,
-22.));
#40172=CARTESIAN_POINT('Ctrl Pts',(0.158531266188313,-18.2019362155735,
-22.));
#40173=CARTESIAN_POINT('Ctrl Pts',(0.0367928950717868,-17.8170936647807,
-22.));
#40174=CARTESIAN_POINT('Ctrl Pts',(-4.16333634234434E-16,-17.5473641762414,
-22.));
#40175=CARTESIAN_POINT('Ctrl Pts',(-4.16333634234434E-16,-17.3205080756888,
-22.));
#40176=CARTESIAN_POINT('Origin',(1.,0.,0.));
#40177=CARTESIAN_POINT('',(0.,17.3205080756888,22.));
#40178=CARTESIAN_POINT('Ctrl Pts',(1.,18.8944436276912,22.));
#40179=CARTESIAN_POINT('Ctrl Pts',(0.893568458572327,18.8944436276912,22.));
#40180=CARTESIAN_POINT('Ctrl Pts',(0.770253263039461,18.8611989035074,22.));
#40181=CARTESIAN_POINT('Ctrl Pts',(0.557443510044933,18.7490875557919,22.));
#40182=CARTESIAN_POINT('Ctrl Pts',(0.439141783764514,18.6399950696597,22.));
#40183=CARTESIAN_POINT('Ctrl Pts',(0.249736801129751,18.3934680475977,22.));
#40184=CARTESIAN_POINT('Ctrl Pts',(0.158531266188312,18.2019362155735,22.));
#40185=CARTESIAN_POINT('Ctrl Pts',(0.0367928950717865,17.8170936647807,
22.));
#40186=CARTESIAN_POINT('Ctrl Pts',(-4.16333634234434E-16,17.5473641762414,
22.));
#40187=CARTESIAN_POINT('Ctrl Pts',(-4.16333634234434E-16,17.3205080756888,
22.));
#40188=CARTESIAN_POINT('',(1.73472347597681E-15,17.3205080756888,-22.));
#40189=CARTESIAN_POINT('Ctrl Pts',(-4.16333634234434E-16,17.3205080756888,
-22.));
#40190=CARTESIAN_POINT('Ctrl Pts',(2.10170270214658E-16,17.5473641762414,
-22.));
#40191=CARTESIAN_POINT('Ctrl Pts',(0.0367928950717868,17.8170936647807,
-22.));
#40192=CARTESIAN_POINT('Ctrl Pts',(0.158531266188313,18.2019362155735,-22.));
#40193=CARTESIAN_POINT('Ctrl Pts',(0.249736801129751,18.3934680475977,-22.));
#40194=CARTESIAN_POINT('Ctrl Pts',(0.439141783764514,18.6399950696597,-22.));
#40195=CARTESIAN_POINT('Ctrl Pts',(0.557443510044933,18.7490875557919,-22.));
#40196=CARTESIAN_POINT('Ctrl Pts',(0.770253263039461,18.8611989035074,-22.));
#40197=CARTESIAN_POINT('Ctrl Pts',(0.893568458572327,18.8944436276912,-22.));
#40198=CARTESIAN_POINT('Ctrl Pts',(1.,18.8944436276912,-22.));
#40199=CARTESIAN_POINT('Origin',(0.,0.,0.));
#40200=CARTESIAN_POINT('Origin',(0.,18.,0.));
#40201=CARTESIAN_POINT('',(0.,18.,22.));
#40202=CARTESIAN_POINT('',(0.,18.,-22.));
#40203=CARTESIAN_POINT('Origin',(-41.,13.,0.));
#40204=CARTESIAN_POINT('Origin',(-40.5,13.,0.));
#40205=CARTESIAN_POINT('Origin',(-41.,12.75,0.));
#40206=CARTESIAN_POINT('Origin',(10.,12.75,0.));
#40207=CARTESIAN_POINT('Origin',(9.5,12.75,0.));
#40208=CARTESIAN_POINT('Origin',(1.73472347597681E-15,29.,-22.));
#40209=CARTESIAN_POINT('Origin',(1.73472347597681E-15,29.,22.));
#66655=UNCERTAINTY_MEASURE_WITH_UNIT(LENGTH_MEASURE(0.01),#66722,
'DISTANCE_ACCURACY_VALUE',
'Maximum model space distance between geometric entities at asserted c
onnectivities');
#66680=UNCERTAINTY_MEASURE_WITH_UNIT(LENGTH_MEASURE(0.01),#66722,
'DISTANCE_ACCURACY_VALUE',
'Maximum model space distance between geometric entities at asserted c
onnectivities');
#66696=(
GEOMETRIC_REPRESENTATION_CONTEXT(3)
GLOBAL_UNCERTAINTY_ASSIGNED_CONTEXT((#66655))
GLOBAL_UNIT_ASSIGNED_CONTEXT((#66722,#66724,#66725))
REPRESENTATION_CONTEXT('','3D')
);
#66721=(
GEOMETRIC_REPRESENTATION_CONTEXT(3)
GLOBAL_UNCERTAINTY_ASSIGNED_CONTEXT((#66680))
GLOBAL_UNIT_ASSIGNED_CONTEXT((#66722,#66724,#66725))
REPRESENTATION_CONTEXT('','3D')
);
#66722=(
LENGTH_UNIT()
NAMED_UNIT(*)
SI_UNIT(.MILLI.,.METRE.)
);
#66724=(
NAMED_UNIT(*)
PLANE_ANGLE_UNIT()
SI_UNIT($,.RADIAN.)
);
#66725=(
NAMED_UNIT(*)
SI_UNIT($,.STERADIAN.)
SOLID_ANGLE_UNIT()
);
#66741=SHAPE_DEFINITION_REPRESENTATION(#66793,#66905);
#66793=PRODUCT_DEFINITION_SHAPE('',$,#66946);
#66905=SHAPE_REPRESENTATION('',(#27328),#66696);
#66930=PRODUCT_DEFINITION_CONTEXT('part definition',#67052,'design');
#66946=PRODUCT_DEFINITION('Ball Screw Nut','Ball Screw Nut',#66986,#66930);
#66986=PRODUCT_DEFINITION_FORMATION('',$,#67069);
#67052=APPLICATION_CONTEXT(
'Core Data for Automotive Mechanical Design Process');
#67053=PRODUCT_CONTEXT('part definition',#67052,'mechanical');
#67069=PRODUCT('Ball Screw Nut','Ball Screw Nut',$,(#67053));
#67095=PRESENTATION_STYLE_ASSIGNMENT((#67097));
#67097=SURFACE_STYLE_USAGE(.BOTH.,#67099);
#67099=SURFACE_SIDE_STYLE('',(#67101));
#67101=SURFACE_STYLE_FILL_AREA(#67103);
#67103=FILL_AREA_STYLE('Opaque(202,209,238)',(#67105));
#67105=FILL_AREA_STYLE_COLOUR('Opaque(202,209,238)',#67107);
#67107=COLOUR_RGB('Opaque(202,209,238)',0.792156862745098,0.819607843137255,
0.933333333333333);
ENDSEC;
END-ISO-10303-21;
